ISO-10303-21;
HEADER;
/* Generated by software containing ST-Developer
 * from STEP Tools, Inc. (www.steptools.com) 
 */

FILE_DESCRIPTION(
/* description */ ('Bearing friction torque test rig'),
/* implementation_level */ '2;1');

FILE_NAME(
/* name */ 'Cap Screw - M5x20.step',
/* time_stamp */ '2026-10-28T03:24:04-07:00',
/* author */ (''),
/* organization */ (''),
/* preprocessor_version */ 'ST-DEVELOPER v20.2',
/* originating_system */ 'Autodesk Translation Framework v15.17.0.0',
/* authorisation */ '');

FILE_SCHEMA (('AUTOMOTIVE_DESIGN { 1 0 10303 214 3 1 1 }'));
ENDSEC;

DATA;
#10=MECHANICAL_DESIGN_GEOMETRIC_PRESENTATION_REPRESENTATION('',(#580),#14822);
#440=CONICAL_SURFACE('',#8887,0.4,0.785398163397448);
#441=CONICAL_SURFACE('',#8891,0.41,0.785398163397448);
#442=CONICAL_SURFACE('',#8895,0.26,0.463647609000806);
#443=CONICAL_SURFACE('',#8899,0.225,0.785398163397448);
#450=ORIENTED_CLOSED_SHELL('',*,#7698,.F.);
#453=BREP_WITH_VOIDS('Body1',#7697,(#450));
#487=SHAPE_REPRESENTATION_RELATIONSHIP('SRR','None',#15028,#526);
#526=ADVANCED_BREP_SHAPE_REPRESENTATION('',(#453),#14808);
#580=STYLED_ITEM('',(#15291),#453);
#832=FACE_BOUND('',#2073,.T.);
#1035=PLANE('',#8885);
#1036=PLANE('',#8893);
#1037=PLANE('',#8901);
#1038=PLANE('',#8902);
#1039=PLANE('',#8903);
#1040=PLANE('',#8904);
#1041=PLANE('',#8905);
#1042=PLANE('',#8906);
#1043=PLANE('',#8907);
#1044=PLANE('',#8908);
#1045=PLANE('',#8909);
#1435=FACE_OUTER_BOUND('',#2068,.T.);
#1436=FACE_OUTER_BOUND('',#2069,.T.);
#1437=FACE_OUTER_BOUND('',#2070,.T.);
#1438=FACE_OUTER_BOUND('',#2071,.T.);
#1439=FACE_OUTER_BOUND('',#2072,.T.);
#1440=FACE_OUTER_BOUND('',#2074,.T.);
#1441=FACE_OUTER_BOUND('',#2075,.T.);
#1442=FACE_OUTER_BOUND('',#2076,.T.);
#1443=FACE_OUTER_BOUND('',#2077,.T.);
#1444=FACE_OUTER_BOUND('',#2078,.T.);
#1445=FACE_OUTER_BOUND('',#2079,.T.);
#1446=FACE_OUTER_BOUND('',#2080,.T.);
#1447=FACE_OUTER_BOUND('',#2081,.T.);
#1448=FACE_OUTER_BOUND('',#2082,.T.);
#1449=FACE_OUTER_BOUND('',#2083,.T.);
#1450=FACE_OUTER_BOUND('',#2084,.T.);
#1451=FACE_OUTER_BOUND('',#2085,.T.);
#2068=EDGE_LOOP('',(#6614));
#2069=EDGE_LOOP('',(#6615,#6616,#6617,#6618));
#2070=EDGE_LOOP('',(#6619,#6620,#6621,#6622));
#2071=EDGE_LOOP('',(#6623,#6624,#6625,#6626));
#2072=EDGE_LOOP('',(#6627));
#2073=EDGE_LOOP('',(#6628));
#2074=EDGE_LOOP('',(#6629,#6630,#6631,#6632));
#2075=EDGE_LOOP('',(#6633,#6634,#6635,#6636));
#2076=EDGE_LOOP('',(#6637,#6638,#6639,#6640));
#2077=EDGE_LOOP('',(#6641));
#2078=EDGE_LOOP('',(#6642,#6643,#6644,#6645));
#2079=EDGE_LOOP('',(#6646,#6647,#6648,#6649));
#2080=EDGE_LOOP('',(#6650,#6651,#6652,#6653));
#2081=EDGE_LOOP('',(#6654,#6655,#6656,#6657));
#2082=EDGE_LOOP('',(#6658,#6659,#6660,#6661));
#2083=EDGE_LOOP('',(#6662,#6663,#6664,#6665));
#2084=EDGE_LOOP('',(#6666,#6667,#6668,#6669,#6670,#6671));
#2085=EDGE_LOOP('',(#6672,#6673,#6674,#6675,#6676,#6677));
#2554=LINE('',#13911,#2998);
#2555=LINE('',#13915,#2999);
#2556=LINE('',#13919,#3000);
#2557=LINE('',#13926,#3001);
#2558=LINE('',#13930,#3002);
#2559=LINE('',#13934,#3003);
#2560=LINE('',#13939,#3004);
#2561=LINE('',#13941,#3005);
#2562=LINE('',#13943,#3006);
#2563=LINE('',#13944,#3007);
#2564=LINE('',#13947,#3008);
#2565=LINE('',#13949,#3009);
#2566=LINE('',#13950,#3010);
#2567=LINE('',#13953,#3011);
#2568=LINE('',#13955,#3012);
#2569=LINE('',#13956,#3013);
#2570=LINE('',#13959,#3014);
#2571=LINE('',#13961,#3015);
#2572=LINE('',#13962,#3016);
#2573=LINE('',#13965,#3017);
#2574=LINE('',#13967,#3018);
#2575=LINE('',#13968,#3019);
#2576=LINE('',#13970,#3020);
#2577=LINE('',#13971,#3021);
#2998=VECTOR('',#10995,0.4);
#2999=VECTOR('',#11000,0.425);
#3000=VECTOR('',#11005,0.41);
#3001=VECTOR('',#11014,0.26);
#3002=VECTOR('',#11019,0.25);
#3003=VECTOR('',#11024,0.225);
#3004=VECTOR('',#11029,1.);
#3005=VECTOR('',#11030,1.);
#3006=VECTOR('',#11031,1.);
#3007=VECTOR('',#11032,1.);
#3008=VECTOR('',#11035,1.);
#3009=VECTOR('',#11036,1.);
#3010=VECTOR('',#11037,1.);
#3011=VECTOR('',#11040,1.);
#3012=VECTOR('',#11041,1.);
#3013=VECTOR('',#11042,1.);
#3014=VECTOR('',#11045,1.);
#3015=VECTOR('',#11046,1.);
#3016=VECTOR('',#11047,1.);
#3017=VECTOR('',#11050,1.);
#3018=VECTOR('',#11051,1.);
#3019=VECTOR('',#11052,1.);
#3020=VECTOR('',#11055,1.);
#3021=VECTOR('',#11056,1.);
#3467=CIRCLE('',#8886,0.375);
#3468=CIRCLE('',#8888,0.425);
#3469=CIRCLE('',#8890,0.425);
#3470=CIRCLE('',#8892,0.395);
#3471=CIRCLE('',#8894,0.27);
#3472=CIRCLE('',#8896,0.24505);
#3473=CIRCLE('',#8898,0.24505);
#3474=CIRCLE('',#8900,0.2);
#4058=VERTEX_POINT('',#13906);
#4059=VERTEX_POINT('',#13909);
#4060=VERTEX_POINT('',#13913);
#4061=VERTEX_POINT('',#13917);
#4062=VERTEX_POINT('',#13921);
#4063=VERTEX_POINT('',#13924);
#4064=VERTEX_POINT('',#13928);
#4065=VERTEX_POINT('',#13932);
#4066=VERTEX_POINT('',#13937);
#4067=VERTEX_POINT('',#13938);
#4068=VERTEX_POINT('',#13940);
#4069=VERTEX_POINT('',#13942);
#4070=VERTEX_POINT('',#13946);
#4071=VERTEX_POINT('',#13948);
#4072=VERTEX_POINT('',#13952);
#4073=VERTEX_POINT('',#13954);
#4074=VERTEX_POINT('',#13958);
#4075=VERTEX_POINT('',#13960);
#4076=VERTEX_POINT('',#13964);
#4077=VERTEX_POINT('',#13966);
#4933=EDGE_CURVE('',#4058,#4058,#3467,.T.);
#4934=EDGE_CURVE('',#4059,#4059,#3468,.T.);
#4935=EDGE_CURVE('',#4059,#4058,#2554,.T.);
#4936=EDGE_CURVE('',#4060,#4060,#3469,.T.);
#4937=EDGE_CURVE('',#4060,#4059,#2555,.T.);
#4938=EDGE_CURVE('',#4061,#4061,#3470,.T.);
#4939=EDGE_CURVE('',#4061,#4060,#2556,.T.);
#4940=EDGE_CURVE('',#4062,#4062,#3471,.T.);
#4941=EDGE_CURVE('',#4063,#4063,#3472,.F.);
#4942=EDGE_CURVE('',#4063,#4062,#2557,.T.);
#4943=EDGE_CURVE('',#4064,#4064,#3473,.F.);
#4944=EDGE_CURVE('',#4064,#4063,#2558,.T.);
#4945=EDGE_CURVE('',#4065,#4065,#3474,.T.);
#4946=EDGE_CURVE('',#4065,#4064,#2559,.T.);
#4947=EDGE_CURVE('',#4066,#4067,#2560,.T.);
#4948=EDGE_CURVE('',#4067,#4068,#2561,.T.);
#4949=EDGE_CURVE('',#4068,#4069,#2562,.T.);
#4950=EDGE_CURVE('',#4066,#4069,#2563,.T.);
#4951=EDGE_CURVE('',#4067,#4070,#2564,.T.);
#4952=EDGE_CURVE('',#4070,#4071,#2565,.T.);
#4953=EDGE_CURVE('',#4071,#4068,#2566,.T.);
#4954=EDGE_CURVE('',#4070,#4072,#2567,.T.);
#4955=EDGE_CURVE('',#4072,#4073,#2568,.T.);
#4956=EDGE_CURVE('',#4073,#4071,#2569,.T.);
#4957=EDGE_CURVE('',#4072,#4074,#2570,.T.);
#4958=EDGE_CURVE('',#4074,#4075,#2571,.T.);
#4959=EDGE_CURVE('',#4075,#4073,#2572,.T.);
#4960=EDGE_CURVE('',#4074,#4076,#2573,.T.);
#4961=EDGE_CURVE('',#4076,#4077,#2574,.T.);
#4962=EDGE_CURVE('',#4077,#4075,#2575,.T.);
#4963=EDGE_CURVE('',#4076,#4066,#2576,.T.);
#4964=EDGE_CURVE('',#4069,#4077,#2577,.T.);
#6614=ORIENTED_EDGE('',*,*,#4933,.F.);
#6615=ORIENTED_EDGE('',*,*,#4934,.F.);
#6616=ORIENTED_EDGE('',*,*,#4935,.T.);
#6617=ORIENTED_EDGE('',*,*,#4933,.T.);
#6618=ORIENTED_EDGE('',*,*,#4935,.F.);
#6619=ORIENTED_EDGE('',*,*,#4936,.F.);
#6620=ORIENTED_EDGE('',*,*,#4937,.T.);
#6621=ORIENTED_EDGE('',*,*,#4934,.T.);
#6622=ORIENTED_EDGE('',*,*,#4937,.F.);
#6623=ORIENTED_EDGE('',*,*,#4938,.F.);
#6624=ORIENTED_EDGE('',*,*,#4939,.T.);
#6625=ORIENTED_EDGE('',*,*,#4936,.T.);
#6626=ORIENTED_EDGE('',*,*,#4939,.F.);
#6627=ORIENTED_EDGE('',*,*,#4938,.T.);
#6628=ORIENTED_EDGE('',*,*,#4940,.F.);
#6629=ORIENTED_EDGE('',*,*,#4941,.F.);
#6630=ORIENTED_EDGE('',*,*,#4942,.T.);
#6631=ORIENTED_EDGE('',*,*,#4940,.T.);
#6632=ORIENTED_EDGE('',*,*,#4942,.F.);
#6633=ORIENTED_EDGE('',*,*,#4943,.F.);
#6634=ORIENTED_EDGE('',*,*,#4944,.T.);
#6635=ORIENTED_EDGE('',*,*,#4941,.T.);
#6636=ORIENTED_EDGE('',*,*,#4944,.F.);
#6637=ORIENTED_EDGE('',*,*,#4945,.F.);
#6638=ORIENTED_EDGE('',*,*,#4946,.T.);
#6639=ORIENTED_EDGE('',*,*,#4943,.T.);
#6640=ORIENTED_EDGE('',*,*,#4946,.F.);
#6641=ORIENTED_EDGE('',*,*,#4945,.T.);
#6642=ORIENTED_EDGE('',*,*,#4947,.T.);
#6643=ORIENTED_EDGE('',*,*,#4948,.T.);
#6644=ORIENTED_EDGE('',*,*,#4949,.T.);
#6645=ORIENTED_EDGE('',*,*,#4950,.F.);
#6646=ORIENTED_EDGE('',*,*,#4951,.T.);
#6647=ORIENTED_EDGE('',*,*,#4952,.T.);
#6648=ORIENTED_EDGE('',*,*,#4953,.T.);
#6649=ORIENTED_EDGE('',*,*,#4948,.F.);
#6650=ORIENTED_EDGE('',*,*,#4954,.T.);
#6651=ORIENTED_EDGE('',*,*,#4955,.T.);
#6652=ORIENTED_EDGE('',*,*,#4956,.T.);
#6653=ORIENTED_EDGE('',*,*,#4952,.F.);
#6654=ORIENTED_EDGE('',*,*,#4957,.T.);
#6655=ORIENTED_EDGE('',*,*,#4958,.T.);
#6656=ORIENTED_EDGE('',*,*,#4959,.T.);
#6657=ORIENTED_EDGE('',*,*,#4955,.F.);
#6658=ORIENTED_EDGE('',*,*,#4960,.T.);
#6659=ORIENTED_EDGE('',*,*,#4961,.T.);
#6660=ORIENTED_EDGE('',*,*,#4962,.T.);
#6661=ORIENTED_EDGE('',*,*,#4958,.F.);
#6662=ORIENTED_EDGE('',*,*,#4963,.T.);
#6663=ORIENTED_EDGE('',*,*,#4950,.T.);
#6664=ORIENTED_EDGE('',*,*,#4964,.T.);
#6665=ORIENTED_EDGE('',*,*,#4961,.F.);
#6666=ORIENTED_EDGE('',*,*,#4963,.F.);
#6667=ORIENTED_EDGE('',*,*,#4960,.F.);
#6668=ORIENTED_EDGE('',*,*,#4957,.F.);
#6669=ORIENTED_EDGE('',*,*,#4954,.F.);
#6670=ORIENTED_EDGE('',*,*,#4951,.F.);
#6671=ORIENTED_EDGE('',*,*,#4947,.F.);
#6672=ORIENTED_EDGE('',*,*,#4964,.F.);
#6673=ORIENTED_EDGE('',*,*,#4949,.F.);
#6674=ORIENTED_EDGE('',*,*,#4953,.F.);
#6675=ORIENTED_EDGE('',*,*,#4956,.F.);
#6676=ORIENTED_EDGE('',*,*,#4959,.F.);
#6677=ORIENTED_EDGE('',*,*,#4962,.F.);
#7174=CYLINDRICAL_SURFACE('',#8889,0.425);
#7175=CYLINDRICAL_SURFACE('',#8897,0.24505);
#7546=ADVANCED_FACE('',(#1435),#1035,.T.);
#7547=ADVANCED_FACE('',(#1436),#440,.T.);
#7548=ADVANCED_FACE('',(#1437),#7174,.T.);
#7549=ADVANCED_FACE('',(#1438),#441,.T.);
#7550=ADVANCED_FACE('',(#1439,#832),#1036,.T.);
#7551=ADVANCED_FACE('',(#1440),#442,.T.);
#7552=ADVANCED_FACE('',(#1441),#7175,.T.);
#7553=ADVANCED_FACE('',(#1442),#443,.T.);
#7554=ADVANCED_FACE('',(#1443),#1037,.T.);
#7555=ADVANCED_FACE('',(#1444),#1038,.F.);
#7556=ADVANCED_FACE('',(#1445),#1039,.F.);
#7557=ADVANCED_FACE('',(#1446),#1040,.F.);
#7558=ADVANCED_FACE('',(#1447),#1041,.F.);
#7559=ADVANCED_FACE('',(#1448),#1042,.F.);
#7560=ADVANCED_FACE('',(#1449),#1043,.F.);
#7561=ADVANCED_FACE('',(#1450),#1044,.F.);
#7562=ADVANCED_FACE('',(#1451),#1045,.F.);
#7697=CLOSED_SHELL('',(#7546,#7547,#7548,#7549,#7550,#7551,#7552,#7553,
#7554));
#7698=CLOSED_SHELL('',(#7555,#7556,#7557,#7558,#7559,#7560,#7561,#7562));
#8884=AXIS2_PLACEMENT_3D('',#13904,#10985,#10986);
#8885=AXIS2_PLACEMENT_3D('',#13905,#10987,#10988);
#8886=AXIS2_PLACEMENT_3D('',#13907,#10989,#10990);
#8887=AXIS2_PLACEMENT_3D('',#13908,#10991,#10992);
#8888=AXIS2_PLACEMENT_3D('',#13910,#10993,#10994);
#8889=AXIS2_PLACEMENT_3D('',#13912,#10996,#10997);
#8890=AXIS2_PLACEMENT_3D('',#13914,#10998,#10999);
#8891=AXIS2_PLACEMENT_3D('',#13916,#11001,#11002);
#8892=AXIS2_PLACEMENT_3D('',#13918,#11003,#11004);
#8893=AXIS2_PLACEMENT_3D('',#13920,#11006,#11007);
#8894=AXIS2_PLACEMENT_3D('',#13922,#11008,#11009);
#8895=AXIS2_PLACEMENT_3D('',#13923,#11010,#11011);
#8896=AXIS2_PLACEMENT_3D('',#13925,#11012,#11013);
#8897=AXIS2_PLACEMENT_3D('',#13927,#11015,#11016);
#8898=AXIS2_PLACEMENT_3D('',#13929,#11017,#11018);
#8899=AXIS2_PLACEMENT_3D('',#13931,#11020,#11021);
#8900=AXIS2_PLACEMENT_3D('',#13933,#11022,#11023);
#8901=AXIS2_PLACEMENT_3D('',#13935,#11025,#11026);
#8902=AXIS2_PLACEMENT_3D('',#13936,#11027,#11028);
#8903=AXIS2_PLACEMENT_3D('',#13945,#11033,#11034);
#8904=AXIS2_PLACEMENT_3D('',#13951,#11038,#11039);
#8905=AXIS2_PLACEMENT_3D('',#13957,#11043,#11044);
#8906=AXIS2_PLACEMENT_3D('',#13963,#11048,#11049);
#8907=AXIS2_PLACEMENT_3D('',#13969,#11053,#11054);
#8908=AXIS2_PLACEMENT_3D('',#13972,#11057,#11058);
#8909=AXIS2_PLACEMENT_3D('',#13973,#11059,#11060);
#10985=DIRECTION('axis',(0.,0.,1.));
#10986=DIRECTION('refdir',(1.,0.,0.));
#10987=DIRECTION('center_axis',(0.,1.,0.));
#10988=DIRECTION('ref_axis',(0.,0.,1.));
#10989=DIRECTION('center_axis',(0.,-1.,0.));
#10990=DIRECTION('ref_axis',(1.,0.,0.));
#10991=DIRECTION('center_axis',(0.,-1.,0.));
#10992=DIRECTION('ref_axis',(1.,0.,0.));
#10993=DIRECTION('center_axis',(0.,-1.,0.));
#10994=DIRECTION('ref_axis',(1.,0.,0.));
#10995=DIRECTION('',(0.707106781186548,0.707106781186547,8.65956056235493E-17));
#10996=DIRECTION('center_axis',(0.,-1.,0.));
#10997=DIRECTION('ref_axis',(1.,0.,0.));
#10998=DIRECTION('center_axis',(0.,-1.,0.));
#10999=DIRECTION('ref_axis',(1.,0.,0.));
#11000=DIRECTION('',(0.,1.,0.));
#11001=DIRECTION('center_axis',(0.,1.,0.));
#11002=DIRECTION('ref_axis',(1.,0.,0.));
#11003=DIRECTION('center_axis',(0.,-1.,0.));
#11004=DIRECTION('ref_axis',(1.,0.,0.));
#11005=DIRECTION('',(-0.707106781186547,0.707106781186548,-8.65956056235493E-17));
#11006=DIRECTION('center_axis',(0.,-1.,0.));
#11007=DIRECTION('ref_axis',(0.,0.,-1.));
#11008=DIRECTION('center_axis',(0.,-1.,0.));
#11009=DIRECTION('ref_axis',(1.,0.,0.));
#11010=DIRECTION('center_axis',(0.,1.,0.));
#11011=DIRECTION('ref_axis',(1.,0.,0.));
#11012=DIRECTION('center_axis',(0.,1.,0.));
#11013=DIRECTION('ref_axis',(1.,0.,0.));
#11014=DIRECTION('',(-0.447213595499958,0.894427190999916,-5.47678698264203E-17));
#11015=DIRECTION('center_axis',(0.,-1.,0.));
#11016=DIRECTION('ref_axis',(1.,0.,0.));
#11017=DIRECTION('center_axis',(0.,1.,0.));
#11018=DIRECTION('ref_axis',(1.,0.,0.));
#11019=DIRECTION('',(0.,1.,0.));
#11020=DIRECTION('center_axis',(0.,1.,0.));
#11021=DIRECTION('ref_axis',(1.,0.,0.));
#11022=DIRECTION('center_axis',(0.,-1.,0.));
#11023=DIRECTION('ref_axis',(1.,0.,0.));
#11024=DIRECTION('',(-0.707106781186547,0.707106781186548,-8.65956056235493E-17));
#11025=DIRECTION('center_axis',(0.,-1.,0.));
#11026=DIRECTION('ref_axis',(0.,0.,-1.));
#11027=DIRECTION('center_axis',(0.866025403784439,0.,-0.5));
#11028=DIRECTION('ref_axis',(0.5,0.,0.866025403784439));
#11029=DIRECTION('',(-0.5,0.,-0.866025403784439));
#11030=DIRECTION('',(0.,-1.,0.));
#11031=DIRECTION('',(0.5,0.,0.866025403784439));
#11032=DIRECTION('',(0.,-1.,0.));
#11033=DIRECTION('center_axis',(1.20185167898973E-16,0.,-1.));
#11034=DIRECTION('ref_axis',(1.,0.,1.20185167898973E-16));
#11035=DIRECTION('',(-1.,0.,-1.20185167898973E-16));
#11036=DIRECTION('',(0.,-1.,0.));
#11037=DIRECTION('',(1.,0.,1.20185167898973E-16));
#11038=DIRECTION('center_axis',(-0.866025403784439,0.,-0.5));
#11039=DIRECTION('ref_axis',(0.5,0.,-0.866025403784439));
#11040=DIRECTION('',(-0.5,0.,0.866025403784439));
#11041=DIRECTION('',(0.,-1.,0.));
#11042=DIRECTION('',(0.5,0.,-0.866025403784439));
#11043=DIRECTION('center_axis',(-0.866025403784439,0.,0.5));
#11044=DIRECTION('ref_axis',(-0.5,0.,-0.866025403784439));
#11045=DIRECTION('',(0.5,0.,0.866025403784439));
#11046=DIRECTION('',(0.,-1.,0.));
#11047=DIRECTION('',(-0.5,0.,-0.866025403784439));
#11048=DIRECTION('center_axis',(-2.40370335797945E-16,0.,1.));
#11049=DIRECTION('ref_axis',(-1.,0.,-2.40370335797945E-16));
#11050=DIRECTION('',(1.,0.,2.40370335797945E-16));
#11051=DIRECTION('',(0.,-1.,0.));
#11052=DIRECTION('',(-1.,0.,-2.40370335797945E-16));
#11053=DIRECTION('center_axis',(0.866025403784439,0.,0.5));
#11054=DIRECTION('ref_axis',(-0.5,0.,0.866025403784439));
#11055=DIRECTION('',(0.5,0.,-0.866025403784439));
#11056=DIRECTION('',(-0.5,0.,0.866025403784439));
#11057=DIRECTION('center_axis',(0.,1.,0.));
#11058=DIRECTION('ref_axis',(1.,0.,0.));
#11059=DIRECTION('center_axis',(0.,-1.,0.));
#11060=DIRECTION('ref_axis',(0.,0.,-1.));
#13904=CARTESIAN_POINT('',(0.,0.,0.));
#13905=CARTESIAN_POINT('Origin',(0.375,0.5,0.));
#13906=CARTESIAN_POINT('',(-0.375,0.5,-4.59242549680257E-17));
#13907=CARTESIAN_POINT('Origin',(0.,0.5,0.));
#13908=CARTESIAN_POINT('Origin',(0.,0.475,0.));
#13909=CARTESIAN_POINT('',(-0.425,0.45,-5.20474889637625E-17));
#13910=CARTESIAN_POINT('Origin',(0.,0.45,0.));
#13911=CARTESIAN_POINT('',(-0.4,0.475,-4.89858719658941E-17));
#13912=CARTESIAN_POINT('Origin',(0.,0.24,0.));
#13913=CARTESIAN_POINT('',(-0.425,0.0299999999999998,-5.20474889637625E-17));
#13914=CARTESIAN_POINT('Origin',(0.,0.0299999999999998,0.));
#13915=CARTESIAN_POINT('',(-0.425,0.24,-5.20474889637625E-17));
#13916=CARTESIAN_POINT('Origin',(0.,0.0150000000000001,0.));
#13917=CARTESIAN_POINT('',(-0.395,4.85722573273506E-17,-4.83735485663204E-17));
#13918=CARTESIAN_POINT('Origin',(0.,0.,0.));
#13919=CARTESIAN_POINT('',(-0.41,0.0150000000000001,-5.02105187650415E-17));
#13920=CARTESIAN_POINT('Origin',(0.27,0.,0.));
#13921=CARTESIAN_POINT('',(-0.27,0.,-3.30654635769785E-17));
#13922=CARTESIAN_POINT('Origin',(0.,0.,0.));
#13923=CARTESIAN_POINT('Origin',(0.,-0.02,0.));
#13924=CARTESIAN_POINT('',(-0.24505,-0.0498999999999999,3.00099698131059E-17));
#13925=CARTESIAN_POINT('Origin',(0.,-0.0498999999999999,0.));
#13926=CARTESIAN_POINT('',(-0.26,-0.02,-3.18408167778312E-17));
#13927=CARTESIAN_POINT('Origin',(0.,-0.995,0.));
#13928=CARTESIAN_POINT('',(-0.24505,-1.95495,3.00099698131059E-17));
#13929=CARTESIAN_POINT('Origin',(0.,-1.95495,0.));
#13930=CARTESIAN_POINT('',(-0.24505,-0.995,-3.00099698131059E-17));
#13931=CARTESIAN_POINT('Origin',(0.,-1.975,0.));
#13932=CARTESIAN_POINT('',(-0.2,-2.,-2.44929359829471E-17));
#13933=CARTESIAN_POINT('Origin',(0.,-2.,0.));
#13934=CARTESIAN_POINT('',(-0.225,-1.975,-2.75545529808154E-17));
#13935=CARTESIAN_POINT('Origin',(0.,-2.,0.));
#13936=CARTESIAN_POINT('Origin',(0.115470053837925,-0.5,-0.2));
#13937=CARTESIAN_POINT('',(0.23094010767585,-0.5,0.));
#13938=CARTESIAN_POINT('',(0.115470053837925,-0.5,-0.2));
#13939=CARTESIAN_POINT('',(0.23094010767585,-0.5,0.));
#13940=CARTESIAN_POINT('',(0.115470053837925,-0.8,-0.2));
#13941=CARTESIAN_POINT('',(0.115470053837925,-0.5,-0.2));
#13942=CARTESIAN_POINT('',(0.23094010767585,-0.8,0.));
#13943=CARTESIAN_POINT('',(0.23094010767585,-0.8,0.));
#13944=CARTESIAN_POINT('',(0.23094010767585,-0.5,0.));
#13945=CARTESIAN_POINT('Origin',(-0.115470053837925,-0.5,-0.2));
#13946=CARTESIAN_POINT('',(-0.115470053837925,-0.5,-0.2));
#13947=CARTESIAN_POINT('',(0.115470053837925,-0.5,-0.2));
#13948=CARTESIAN_POINT('',(-0.115470053837925,-0.8,-0.2));
#13949=CARTESIAN_POINT('',(-0.115470053837925,-0.5,-0.2));
#13950=CARTESIAN_POINT('',(0.115470053837925,-0.8,-0.2));
#13951=CARTESIAN_POINT('Origin',(-0.23094010767585,-0.5,-2.77555756156289E-17));
#13952=CARTESIAN_POINT('',(-0.23094010767585,-0.5,-2.82820063659975E-17));
#13953=CARTESIAN_POINT('',(-0.115470053837925,-0.5,-0.2));
#13954=CARTESIAN_POINT('',(-0.23094010767585,-0.8,-2.77555756156289E-17));
#13955=CARTESIAN_POINT('',(-0.23094010767585,-0.5,-2.82820063659975E-17));
#13956=CARTESIAN_POINT('',(-0.115470053837925,-0.8,-0.2));
#13957=CARTESIAN_POINT('Origin',(-0.115470053837925,-0.5,0.2));
#13958=CARTESIAN_POINT('',(-0.115470053837925,-0.5,0.2));
#13959=CARTESIAN_POINT('',(-0.23094010767585,-0.5,-2.82820063659975E-17));
#13960=CARTESIAN_POINT('',(-0.115470053837925,-0.8,0.2));
#13961=CARTESIAN_POINT('',(-0.115470053837925,-0.5,0.2));
#13962=CARTESIAN_POINT('',(-0.23094010767585,-0.8,-2.82820063659975E-17));
#13963=CARTESIAN_POINT('Origin',(0.115470053837925,-0.5,0.2));
#13964=CARTESIAN_POINT('',(0.115470053837925,-0.5,0.2));
#13965=CARTESIAN_POINT('',(-0.115470053837925,-0.5,0.2));
#13966=CARTESIAN_POINT('',(0.115470053837925,-0.8,0.2));
#13967=CARTESIAN_POINT('',(0.115470053837925,-0.5,0.2));
#13968=CARTESIAN_POINT('',(-0.115470053837925,-0.8,0.2));
#13969=CARTESIAN_POINT('Origin',(0.23094010767585,-0.5,0.));
#13970=CARTESIAN_POINT('',(0.115470053837925,-0.5,0.2));
#13971=CARTESIAN_POINT('',(0.115470053837925,-0.8,0.2));
#13972=CARTESIAN_POINT('Origin',(0.,-0.5,0.));
#13973=CARTESIAN_POINT('Origin',(0.,-0.8,0.));
#14763=UNCERTAINTY_MEASURE_WITH_UNIT(LENGTH_MEASURE(0.001),#14823,
'DISTANCE_ACCURACY_VALUE',
'Maximum model space distance between geometric entities at asserted c
onnectivities');
#14777=UNCERTAINTY_MEASURE_WITH_UNIT(LENGTH_MEASURE(0.001),#14823,
'DISTANCE_ACCURACY_VALUE',
'Maximum model space distance between geometric entities at asserted c
onnectivities');
#14808=(
GEOMETRIC_REPRESENTATION_CONTEXT(3)
GLOBAL_UNCERTAINTY_ASSIGNED_CONTEXT((#14763))
GLOBAL_UNIT_ASSIGNED_CONTEXT((#14823,#14825,#14826))
REPRESENTATION_CONTEXT('','3D')
);
#14822=(
GEOMETRIC_REPRESENTATION_CONTEXT(3)
GLOBAL_UNCERTAINTY_ASSIGNED_CONTEXT((#14777))
GLOBAL_UNIT_ASSIGNED_CONTEXT((#14823,#14825,#14826))
REPRESENTATION_CONTEXT('','3D')
);
#14823=(
LENGTH_UNIT()
NAMED_UNIT(*)
SI_UNIT(.CENTI.,.METRE.)
);
#14825=(
NAMED_UNIT(*)
PLANE_ANGLE_UNIT()
SI_UNIT($,.RADIAN.)
);
#14826=(
NAMED_UNIT(*)
SI_UNIT($,.STERADIAN.)
SOLID_ANGLE_UNIT()
);
#14857=SHAPE_DEFINITION_REPRESENTATION(#14911,#15028);
#14911=PRODUCT_DEFINITION_SHAPE('',$,#15073);
#15028=SHAPE_REPRESENTATION('',(#8884),#14808);
#15042=PRODUCT_DEFINITION_CONTEXT('part definition',#15176,'design');
#15073=PRODUCT_DEFINITION('Cap Screw - M5x20','Cap Screw - M5x20',#15117,
#15042);
#15117=PRODUCT_DEFINITION_FORMATION('',$,#15208);
#15176=APPLICATION_CONTEXT(
'Core Data for Automotive Mechanical Design Process');
#15177=PRODUCT_CONTEXT('part definition',#15176,'mechanical');
#15208=PRODUCT('Cap Screw - M5x20','Cap Screw - M5x20',
'Cap Screw - M5x20',(#15177));
#15285=COLOUR_RGB('Black',0.12,0.14,0.17);
#15286=FILL_AREA_STYLE_COLOUR('',#15285);
#15287=FILL_AREA_STYLE('',(#15286));
#15288=SURFACE_STYLE_FILL_AREA(#15287);
#15289=SURFACE_SIDE_STYLE('',(#15288));
#15290=SURFACE_STYLE_USAGE(.BOTH.,#15289);
#15291=PRESENTATION_STYLE_ASSIGNMENT((#15290));
ENDSEC;
END-ISO-10303-21;
